ISO-10303-21;
HEADER;
/* Generated by software containing ST-Developer
 * from STEP Tools, Inc. (www.steptools.com) 
 */

FILE_DESCRIPTION(
/* description */ (''),
/* implementation_level */ '2;1');

FILE_NAME(
/* name */ 'Main_Housing.step',
/* time_stamp */ '2026-10-23T17:22:31+06:00',
/* author */ (''),
/* organization */ (''),
/* preprocessor_version */ 'ST-DEVELOPER v20.2',
/* originating_system */ 'Autodesk Translation Framework v15.15.0.0',
/* authorisation */ '');

FILE_SCHEMA (('AUTOMOTIVE_DESIGN { 1 0 10303 214 3 1 1 }'));
ENDSEC;

DATA;
#10=MECHANICAL_DESIGN_GEOMETRIC_PRESENTATION_REPRESENTATION('',(#81),#7315);
#61=SHAPE_REPRESENTATION_RELATIONSHIP('SRR','None',#7357,#71);
#71=ADVANCED_BREP_SHAPE_REPRESENTATION('',(#91),#7309);
#81=STYLED_ITEM('',(#7424),#91);
#91=MANIFOLD_SOLID_BREP('Main_Housing',#3218);
#103=CONICAL_SURFACE('',#3651,4.47286361298787,0.785398163397448);
#220=B_SPLINE_CURVE_WITH_KNOTS('',3,(#7037,#7038,#7039,#7040,#7041,#7042,
#7043,#7044,#7045,#7046,#7047,#7048,#7049,#7050,#7051,#7052,#7053,#7054),
 .UNSPECIFIED.,.F.,.F.,(4,2,2,2,2,2,2,2,4),(0.,0.0376986977587122,0.0753973955174244,
0.11309593596243,0.150794476407437,0.188493016852443,0.226191557297449,
0.263890255056161,0.301588952814873),.UNSPECIFIED.);
#221=B_SPLINE_CURVE_WITH_KNOTS('',3,(#7057,#7058,#7059,#7060,#7061,#7062,
#7063,#7064,#7065,#7066,#7067,#7068,#7069,#7070,#7071,#7072,#7073,#7074),
 .UNSPECIFIED.,.F.,.F.,(4,2,2,2,2,2,2,2,4),(-0.301588952814873,-0.263890255056161,
-0.226191557297449,-0.188493016852443,-0.150794476407437,-0.113095935962431,
-0.0753973955174246,-0.0376986977587124,0.),.UNSPECIFIED.);
#222=B_SPLINE_CURVE_WITH_KNOTS('',3,(#7085,#7086,#7087,#7088,#7089,#7090,
#7091,#7092,#7093,#7094),.UNSPECIFIED.,.F.,.F.,(4,2,2,2,4),(-0.150763619405615,
-0.113072757903898,-0.0753818964021818,-0.037690948201091,0.),
 .UNSPECIFIED.);
#223=B_SPLINE_CURVE_WITH_KNOTS('',3,(#7095,#7096,#7097,#7098,#7099,#7100,
#7101,#7102,#7103,#7104),.UNSPECIFIED.,.F.,.F.,(4,2,2,2,4),(-0.30152723881123,
-0.263836290610139,-0.226145342409048,-0.188454480907332,-0.150763619405615),
 .UNSPECIFIED.);
#224=B_SPLINE_CURVE_WITH_KNOTS('',3,(#7108,#7109,#7110,#7111,#7112,#7113,
#7114,#7115,#7116,#7117),.UNSPECIFIED.,.F.,.F.,(4,2,2,2,4),(0.,0.037690948201091,
0.075381896402182,0.113072757903899,0.150763619405615),.UNSPECIFIED.);
#225=B_SPLINE_CURVE_WITH_KNOTS('',3,(#7119,#7120,#7121,#7122,#7123,#7124,
#7125,#7126,#7127,#7128),.UNSPECIFIED.,.F.,.F.,(4,2,2,2,4),(0.452290858216846,
0.489981719718562,0.527672581220279,0.56536352942137,0.603054477622461),
 .UNSPECIFIED.);
#226=B_SPLINE_CURVE_WITH_KNOTS('',3,(#7132,#7133,#7134,#7135,#7136,#7137,
#7138,#7139,#7140,#7141,#7142,#7143,#7144,#7145,#7146,#7147,#7148,#7149),
 .UNSPECIFIED.,.F.,.F.,(4,2,2,2,2,2,2,2,4),(0.150763619405615,0.188454480907332,
0.226145342409048,0.263836290610139,0.30152723881123,0.339218187012321,
0.376909135213412,0.414599996715129,0.452290858216846),.UNSPECIFIED.);
#227=B_SPLINE_CURVE_WITH_KNOTS('',3,(#7157,#7158,#7159,#7160,#7161,#7162,
#7163,#7164,#7165,#7166),.UNSPECIFIED.,.F.,.F.,(4,2,2,2,4),(0.150763619405615,
0.188454480907332,0.226145342409048,0.263836290610139,0.30152723881123),
 .UNSPECIFIED.);
#228=B_SPLINE_CURVE_WITH_KNOTS('',3,(#7167,#7168,#7169,#7170,#7171,#7172,
#7173,#7174,#7175,#7176),.UNSPECIFIED.,.F.,.F.,(4,2,2,2,4),(0.,0.037690948201091,
0.075381896402182,0.113072757903899,0.150763619405615),.UNSPECIFIED.);
#366=LINE('',#7029,#526);
#367=LINE('',#7035,#527);
#368=LINE('',#7056,#528);
#369=LINE('',#7077,#529);
#370=LINE('',#7079,#530);
#371=LINE('',#7080,#531);
#372=LINE('',#7083,#532);
#373=LINE('',#7130,#533);
#374=LINE('',#7153,#534);
#375=LINE('',#7154,#535);
#376=LINE('',#7183,#536);
#377=LINE('',#7191,#537);
#378=LINE('',#7199,#538);
#379=LINE('',#7200,#539);
#380=LINE('',#7202,#540);
#381=LINE('',#7214,#541);
#526=VECTOR('',#4475,9.50579594738959);
#527=VECTOR('',#4480,10.);
#528=VECTOR('',#4481,10.);
#529=VECTOR('',#4484,10.);
#530=VECTOR('',#4485,10.);
#531=VECTOR('',#4486,10.);
#532=VECTOR('',#4489,10.);
#533=VECTOR('',#4492,1.);
#534=VECTOR('',#4499,10.);
#535=VECTOR('',#4500,10.);
#536=VECTOR('',#4509,4.47286361298787);
#537=VECTOR('',#4520,4.72286361298787);
#538=VECTOR('',#4531,11.0246348408465);
#539=VECTOR('',#4532,11.0246348408465);
#540=VECTOR('',#4533,11.0246348408465);
#541=VECTOR('',#4552,3.72286361298787);
#676=CYLINDRICAL_SURFACE('',#3639,9.50579594738959);
#677=CYLINDRICAL_SURFACE('',#3645,1.);
#678=CYLINDRICAL_SURFACE('',#3646,1.);
#679=CYLINDRICAL_SURFACE('',#3650,1.);
#680=CYLINDRICAL_SURFACE('',#3657,4.72286361298787);
#681=CYLINDRICAL_SURFACE('',#3663,11.0246348408465);
#682=CYLINDRICAL_SURFACE('',#3672,3.72286361298787);
#691=FACE_BOUND('',#1060,.T.);
#692=FACE_BOUND('',#1069,.T.);
#693=FACE_BOUND('',#1074,.T.);
#694=FACE_BOUND('',#1077,.T.);
#695=FACE_BOUND('',#1079,.T.);
#712=PLANE('',#3644);
#713=PLANE('',#3648);
#714=PLANE('',#3649);
#715=PLANE('',#3655);
#716=PLANE('',#3665);
#717=PLANE('',#3669);
#718=PLANE('',#3670);
#875=FACE_OUTER_BOUND('',#1059,.T.);
#876=FACE_OUTER_BOUND('',#1061,.T.);
#877=FACE_OUTER_BOUND('',#1062,.T.);
#878=FACE_OUTER_BOUND('',#1063,.T.);
#879=FACE_OUTER_BOUND('',#1064,.T.);
#880=FACE_OUTER_BOUND('',#1065,.T.);
#881=FACE_OUTER_BOUND('',#1066,.T.);
#882=FACE_OUTER_BOUND('',#1067,.T.);
#883=FACE_OUTER_BOUND('',#1068,.T.);
#884=FACE_OUTER_BOUND('',#1070,.T.);
#885=FACE_OUTER_BOUND('',#1071,.T.);
#886=FACE_OUTER_BOUND('',#1072,.T.);
#887=FACE_OUTER_BOUND('',#1073,.T.);
#888=FACE_OUTER_BOUND('',#1075,.T.);
#889=FACE_OUTER_BOUND('',#1076,.T.);
#890=FACE_OUTER_BOUND('',#1078,.T.);
#891=FACE_OUTER_BOUND('',#1080,.T.);
#1059=EDGE_LOOP('',(#2894,#2895,#2896,#2897,#2898,#2899));
#1060=EDGE_LOOP('',(#2900,#2901,#2902,#2903));
#1061=EDGE_LOOP('',(#2904,#2905,#2906,#2907));
#1062=EDGE_LOOP('',(#2908,#2909,#2910,#2911,#2912));
#1063=EDGE_LOOP('',(#2913,#2914,#2915,#2916,#2917,#2918));
#1064=EDGE_LOOP('',(#2919));
#1065=EDGE_LOOP('',(#2920,#2921,#2922,#2923));
#1066=EDGE_LOOP('',(#2924,#2925,#2926,#2927,#2928));
#1067=EDGE_LOOP('',(#2929,#2930,#2931,#2932,#2933));
#1068=EDGE_LOOP('',(#2934));
#1069=EDGE_LOOP('',(#2935));
#1070=EDGE_LOOP('',(#2936,#2937,#2938,#2939,#2940));
#1071=EDGE_LOOP('',(#2941,#2942,#2943,#2944));
#1072=EDGE_LOOP('',(#2945,#2946,#2947,#2948,#2949,#2950,#2951,#2952,#2953,
#2954,#2955,#2956,#2957,#2958,#2959,#2960,#2961));
#1073=EDGE_LOOP('',(#2962));
#1074=EDGE_LOOP('',(#2963,#2964));
#1075=EDGE_LOOP('',(#2965,#2966,#2967,#2968));
#1076=EDGE_LOOP('',(#2969));
#1077=EDGE_LOOP('',(#2970));
#1078=EDGE_LOOP('',(#2971,#2972));
#1079=EDGE_LOOP('',(#2973));
#1080=EDGE_LOOP('',(#2974,#2975,#2976,#2977));
#1254=CIRCLE('',#3640,9.50563484084649);
#1255=CIRCLE('',#3641,9.50563484084649);
#1256=CIRCLE('',#3642,9.50563484084649);
#1257=CIRCLE('',#3643,9.50563484084649);
#1258=CIRCLE('',#3647,1.);
#1259=CIRCLE('',#3652,4.72286361298787);
#1260=CIRCLE('',#3653,4.72286361298787);
#1261=CIRCLE('',#3654,4.22286361298787);
#1262=CIRCLE('',#3656,3.72286361298787);
#1263=CIRCLE('',#3658,4.72286361298787);
#1264=CIRCLE('',#3660,10.5246348408465);
#1265=CIRCLE('',#3661,0.5);
#1266=CIRCLE('',#3662,11.0246348408465);
#1267=CIRCLE('',#3664,11.0246348408465);
#1268=CIRCLE('',#3667,0.5);
#1269=CIRCLE('',#3668,10.5246348408465);
#1270=CIRCLE('',#3671,3.72286361298787);
#1559=VERTEX_POINT('',#7024);
#1560=VERTEX_POINT('',#7025);
#1561=VERTEX_POINT('',#7028);
#1562=VERTEX_POINT('',#7030);
#1563=VERTEX_POINT('',#7033);
#1564=VERTEX_POINT('',#7034);
#1565=VERTEX_POINT('',#7036);
#1566=VERTEX_POINT('',#7055);
#1567=VERTEX_POINT('',#7076);
#1568=VERTEX_POINT('',#7078);
#1569=VERTEX_POINT('',#7082);
#1570=VERTEX_POINT('',#7084);
#1571=VERTEX_POINT('',#7106);
#1572=VERTEX_POINT('',#7107);
#1573=VERTEX_POINT('',#7118);
#1574=VERTEX_POINT('',#7129);
#1575=VERTEX_POINT('',#7152);
#1576=VERTEX_POINT('',#7156);
#1577=VERTEX_POINT('',#7178);
#1578=VERTEX_POINT('',#7179);
#1579=VERTEX_POINT('',#7182);
#1580=VERTEX_POINT('',#7186);
#1581=VERTEX_POINT('',#7189);
#1582=VERTEX_POINT('',#7193);
#1583=VERTEX_POINT('',#7195);
#1584=VERTEX_POINT('',#7201);
#1585=VERTEX_POINT('',#7206);
#1586=VERTEX_POINT('',#7211);
#2013=EDGE_CURVE('',#1559,#1560,#1254,.T.);
#2014=EDGE_CURVE('',#1560,#1559,#1255,.T.);
#2015=EDGE_CURVE('',#1559,#1561,#366,.T.);
#2016=EDGE_CURVE('',#1562,#1561,#1256,.T.);
#2017=EDGE_CURVE('',#1561,#1562,#1257,.T.);
#2018=EDGE_CURVE('',#1563,#1564,#367,.T.);
#2019=EDGE_CURVE('',#1565,#1563,#220,.T.);
#2020=EDGE_CURVE('',#1566,#1565,#368,.T.);
#2021=EDGE_CURVE('',#1564,#1566,#221,.T.);
#2022=EDGE_CURVE('',#1565,#1567,#369,.T.);
#2023=EDGE_CURVE('',#1568,#1567,#370,.T.);
#2024=EDGE_CURVE('',#1566,#1568,#371,.T.);
#2025=EDGE_CURVE('',#1563,#1569,#372,.T.);
#2026=EDGE_CURVE('',#1570,#1569,#222,.T.);
#2027=EDGE_CURVE('',#1567,#1570,#223,.T.);
#2028=EDGE_CURVE('',#1571,#1572,#224,.T.);
#2029=EDGE_CURVE('',#1573,#1571,#225,.T.);
#2030=EDGE_CURVE('',#1573,#1574,#373,.T.);
#2031=EDGE_CURVE('',#1574,#1574,#1258,.T.);
#2032=EDGE_CURVE('',#1572,#1573,#226,.T.);
#2033=EDGE_CURVE('',#1564,#1575,#374,.T.);
#2034=EDGE_CURVE('',#1569,#1575,#375,.T.);
#2035=EDGE_CURVE('',#1576,#1568,#227,.T.);
#2036=EDGE_CURVE('',#1575,#1576,#228,.T.);
#2037=EDGE_CURVE('',#1577,#1578,#1259,.T.);
#2038=EDGE_CURVE('',#1578,#1577,#1260,.T.);
#2039=EDGE_CURVE('',#1577,#1579,#376,.T.);
#2040=EDGE_CURVE('',#1579,#1579,#1261,.T.);
#2041=EDGE_CURVE('',#1580,#1580,#1262,.T.);
#2042=EDGE_CURVE('',#1581,#1581,#1263,.T.);
#2043=EDGE_CURVE('',#1581,#1578,#377,.T.);
#2044=EDGE_CURVE('',#1582,#1582,#1264,.T.);
#2045=EDGE_CURVE('',#1582,#1583,#1265,.T.);
#2046=EDGE_CURVE('',#1583,#1583,#1266,.T.);
#2047=EDGE_CURVE('',#1583,#1570,#378,.T.);
#2048=EDGE_CURVE('',#1576,#1572,#379,.T.);
#2049=EDGE_CURVE('',#1573,#1584,#380,.T.);
#2050=EDGE_CURVE('',#1584,#1584,#1267,.T.);
#2051=EDGE_CURVE('',#1584,#1585,#1268,.T.);
#2052=EDGE_CURVE('',#1585,#1585,#1269,.T.);
#2053=EDGE_CURVE('',#1586,#1586,#1270,.T.);
#2054=EDGE_CURVE('',#1586,#1580,#381,.T.);
#2894=ORIENTED_EDGE('',*,*,#2013,.T.);
#2895=ORIENTED_EDGE('',*,*,#2014,.T.);
#2896=ORIENTED_EDGE('',*,*,#2015,.T.);
#2897=ORIENTED_EDGE('',*,*,#2016,.F.);
#2898=ORIENTED_EDGE('',*,*,#2017,.F.);
#2899=ORIENTED_EDGE('',*,*,#2015,.F.);
#2900=ORIENTED_EDGE('',*,*,#2018,.F.);
#2901=ORIENTED_EDGE('',*,*,#2019,.F.);
#2902=ORIENTED_EDGE('',*,*,#2020,.F.);
#2903=ORIENTED_EDGE('',*,*,#2021,.F.);
#2904=ORIENTED_EDGE('',*,*,#2020,.T.);
#2905=ORIENTED_EDGE('',*,*,#2022,.T.);
#2906=ORIENTED_EDGE('',*,*,#2023,.F.);
#2907=ORIENTED_EDGE('',*,*,#2024,.F.);
#2908=ORIENTED_EDGE('',*,*,#2019,.T.);
#2909=ORIENTED_EDGE('',*,*,#2025,.T.);
#2910=ORIENTED_EDGE('',*,*,#2026,.F.);
#2911=ORIENTED_EDGE('',*,*,#2027,.F.);
#2912=ORIENTED_EDGE('',*,*,#2022,.F.);
#2913=ORIENTED_EDGE('',*,*,#2028,.F.);
#2914=ORIENTED_EDGE('',*,*,#2029,.F.);
#2915=ORIENTED_EDGE('',*,*,#2030,.T.);
#2916=ORIENTED_EDGE('',*,*,#2031,.T.);
#2917=ORIENTED_EDGE('',*,*,#2030,.F.);
#2918=ORIENTED_EDGE('',*,*,#2032,.F.);
#2919=ORIENTED_EDGE('',*,*,#2031,.F.);
#2920=ORIENTED_EDGE('',*,*,#2018,.T.);
#2921=ORIENTED_EDGE('',*,*,#2033,.T.);
#2922=ORIENTED_EDGE('',*,*,#2034,.F.);
#2923=ORIENTED_EDGE('',*,*,#2025,.F.);
#2924=ORIENTED_EDGE('',*,*,#2021,.T.);
#2925=ORIENTED_EDGE('',*,*,#2024,.T.);
#2926=ORIENTED_EDGE('',*,*,#2035,.F.);
#2927=ORIENTED_EDGE('',*,*,#2036,.F.);
#2928=ORIENTED_EDGE('',*,*,#2033,.F.);
#2929=ORIENTED_EDGE('',*,*,#2037,.T.);
#2930=ORIENTED_EDGE('',*,*,#2038,.T.);
#2931=ORIENTED_EDGE('',*,*,#2039,.T.);
#2932=ORIENTED_EDGE('',*,*,#2040,.T.);
#2933=ORIENTED_EDGE('',*,*,#2039,.F.);
#2934=ORIENTED_EDGE('',*,*,#2040,.F.);
#2935=ORIENTED_EDGE('',*,*,#2041,.T.);
#2936=ORIENTED_EDGE('',*,*,#2042,.F.);
#2937=ORIENTED_EDGE('',*,*,#2043,.T.);
#2938=ORIENTED_EDGE('',*,*,#2037,.F.);
#2939=ORIENTED_EDGE('',*,*,#2038,.F.);
#2940=ORIENTED_EDGE('',*,*,#2043,.F.);
#2941=ORIENTED_EDGE('',*,*,#2044,.T.);
#2942=ORIENTED_EDGE('',*,*,#2045,.T.);
#2943=ORIENTED_EDGE('',*,*,#2046,.T.);
#2944=ORIENTED_EDGE('',*,*,#2045,.F.);
#2945=ORIENTED_EDGE('',*,*,#2046,.F.);
#2946=ORIENTED_EDGE('',*,*,#2047,.T.);
#2947=ORIENTED_EDGE('',*,*,#2026,.T.);
#2948=ORIENTED_EDGE('',*,*,#2034,.T.);
#2949=ORIENTED_EDGE('',*,*,#2036,.T.);
#2950=ORIENTED_EDGE('',*,*,#2048,.T.);
#2951=ORIENTED_EDGE('',*,*,#2032,.T.);
#2952=ORIENTED_EDGE('',*,*,#2049,.T.);
#2953=ORIENTED_EDGE('',*,*,#2050,.F.);
#2954=ORIENTED_EDGE('',*,*,#2049,.F.);
#2955=ORIENTED_EDGE('',*,*,#2029,.T.);
#2956=ORIENTED_EDGE('',*,*,#2028,.T.);
#2957=ORIENTED_EDGE('',*,*,#2048,.F.);
#2958=ORIENTED_EDGE('',*,*,#2035,.T.);
#2959=ORIENTED_EDGE('',*,*,#2023,.T.);
#2960=ORIENTED_EDGE('',*,*,#2027,.T.);
#2961=ORIENTED_EDGE('',*,*,#2047,.F.);
#2962=ORIENTED_EDGE('',*,*,#2044,.F.);
#2963=ORIENTED_EDGE('',*,*,#2014,.F.);
#2964=ORIENTED_EDGE('',*,*,#2013,.F.);
#2965=ORIENTED_EDGE('',*,*,#2050,.T.);
#2966=ORIENTED_EDGE('',*,*,#2051,.T.);
#2967=ORIENTED_EDGE('',*,*,#2052,.T.);
#2968=ORIENTED_EDGE('',*,*,#2051,.F.);
#2969=ORIENTED_EDGE('',*,*,#2052,.F.);
#2970=ORIENTED_EDGE('',*,*,#2042,.T.);
#2971=ORIENTED_EDGE('',*,*,#2016,.T.);
#2972=ORIENTED_EDGE('',*,*,#2017,.T.);
#2973=ORIENTED_EDGE('',*,*,#2053,.F.);
#2974=ORIENTED_EDGE('',*,*,#2053,.T.);
#2975=ORIENTED_EDGE('',*,*,#2054,.T.);
#2976=ORIENTED_EDGE('',*,*,#2041,.F.);
#2977=ORIENTED_EDGE('',*,*,#2054,.F.);
#3030=TOROIDAL_SURFACE('',#3659,10.5246348408465,0.5);
#3031=TOROIDAL_SURFACE('',#3666,10.5246348408465,0.5);
#3179=ADVANCED_FACE('',(#875,#691),#676,.F.);
#3180=ADVANCED_FACE('',(#876),#712,.F.);
#3181=ADVANCED_FACE('',(#877),#677,.F.);
#3182=ADVANCED_FACE('',(#878),#678,.F.);
#3183=ADVANCED_FACE('',(#879),#713,.T.);
#3184=ADVANCED_FACE('',(#880),#714,.F.);
#3185=ADVANCED_FACE('',(#881),#679,.F.);
#3186=ADVANCED_FACE('',(#882),#103,.T.);
#3187=ADVANCED_FACE('',(#883,#692),#715,.T.);
#3188=ADVANCED_FACE('',(#884),#680,.T.);
#3189=ADVANCED_FACE('',(#885),#3030,.T.);
#3190=ADVANCED_FACE('',(#886),#681,.T.);
#3191=ADVANCED_FACE('',(#887,#693),#716,.T.);
#3192=ADVANCED_FACE('',(#888),#3031,.T.);
#3193=ADVANCED_FACE('',(#889,#694),#717,.T.);
#3194=ADVANCED_FACE('',(#890,#695),#718,.T.);
#3195=ADVANCED_FACE('',(#891),#682,.F.);
#3218=CLOSED_SHELL('',(#3179,#3180,#3181,#3182,#3183,#3184,#3185,#3186,
#3187,#3188,#3189,#3190,#3191,#3192,#3193,#3194,#3195));
#3638=AXIS2_PLACEMENT_3D('',#7022,#4467,#4468);
#3639=AXIS2_PLACEMENT_3D('',#7023,#4469,#4470);
#3640=AXIS2_PLACEMENT_3D('',#7026,#4471,#4472);
#3641=AXIS2_PLACEMENT_3D('',#7027,#4473,#4474);
#3642=AXIS2_PLACEMENT_3D('',#7031,#4476,#4477);
#3643=AXIS2_PLACEMENT_3D('',#7032,#4478,#4479);
#3644=AXIS2_PLACEMENT_3D('',#7075,#4482,#4483);
#3645=AXIS2_PLACEMENT_3D('',#7081,#4487,#4488);
#3646=AXIS2_PLACEMENT_3D('',#7105,#4490,#4491);
#3647=AXIS2_PLACEMENT_3D('',#7131,#4493,#4494);
#3648=AXIS2_PLACEMENT_3D('',#7150,#4495,#4496);
#3649=AXIS2_PLACEMENT_3D('',#7151,#4497,#4498);
#3650=AXIS2_PLACEMENT_3D('',#7155,#4501,#4502);
#3651=AXIS2_PLACEMENT_3D('',#7177,#4503,#4504);
#3652=AXIS2_PLACEMENT_3D('',#7180,#4505,#4506);
#3653=AXIS2_PLACEMENT_3D('',#7181,#4507,#4508);
#3654=AXIS2_PLACEMENT_3D('',#7184,#4510,#4511);
#3655=AXIS2_PLACEMENT_3D('',#7185,#4512,#4513);
#3656=AXIS2_PLACEMENT_3D('',#7187,#4514,#4515);
#3657=AXIS2_PLACEMENT_3D('',#7188,#4516,#4517);
#3658=AXIS2_PLACEMENT_3D('',#7190,#4518,#4519);
#3659=AXIS2_PLACEMENT_3D('',#7192,#4521,#4522);
#3660=AXIS2_PLACEMENT_3D('',#7194,#4523,#4524);
#3661=AXIS2_PLACEMENT_3D('',#7196,#4525,#4526);
#3662=AXIS2_PLACEMENT_3D('',#7197,#4527,#4528);
#3663=AXIS2_PLACEMENT_3D('',#7198,#4529,#4530);
#3664=AXIS2_PLACEMENT_3D('',#7203,#4534,#4535);
#3665=AXIS2_PLACEMENT_3D('',#7204,#4536,#4537);
#3666=AXIS2_PLACEMENT_3D('',#7205,#4538,#4539);
#3667=AXIS2_PLACEMENT_3D('',#7207,#4540,#4541);
#3668=AXIS2_PLACEMENT_3D('',#7208,#4542,#4543);
#3669=AXIS2_PLACEMENT_3D('',#7209,#4544,#4545);
#3670=AXIS2_PLACEMENT_3D('',#7210,#4546,#4547);
#3671=AXIS2_PLACEMENT_3D('',#7212,#4548,#4549);
#3672=AXIS2_PLACEMENT_3D('',#7213,#4550,#4551);
#4467=DIRECTION('axis',(0.,0.,1.));
#4468=DIRECTION('refdir',(1.,0.,0.));
#4469=DIRECTION('center_axis',(-1.,0.,0.));
#4470=DIRECTION('ref_axis',(0.,-1.,0.));
#4471=DIRECTION('center_axis',(1.,0.,0.));
#4472=DIRECTION('ref_axis',(0.,0.,-1.));
#4473=DIRECTION('center_axis',(1.,0.,0.));
#4474=DIRECTION('ref_axis',(0.,0.,-1.));
#4475=DIRECTION('',(-1.,0.,0.));
#4476=DIRECTION('center_axis',(1.,0.,0.));
#4477=DIRECTION('ref_axis',(0.,0.,-1.));
#4478=DIRECTION('center_axis',(1.,0.,0.));
#4479=DIRECTION('ref_axis',(0.,0.,-1.));
#4480=DIRECTION('',(-1.,0.,0.));
#4481=DIRECTION('',(1.,0.,0.));
#4482=DIRECTION('center_axis',(0.,1.,0.));
#4483=DIRECTION('ref_axis',(-1.,0.,0.));
#4484=DIRECTION('',(0.,0.,1.));
#4485=DIRECTION('',(1.,0.,0.));
#4486=DIRECTION('',(0.,0.,1.));
#4487=DIRECTION('center_axis',(0.,0.,1.));
#4488=DIRECTION('ref_axis',(0.,-1.,0.));
#4489=DIRECTION('',(0.,0.,1.));
#4490=DIRECTION('center_axis',(0.,0.,-1.));
#4491=DIRECTION('ref_axis',(1.,0.,0.));
#4492=DIRECTION('',(0.,0.,-1.));
#4493=DIRECTION('center_axis',(0.,0.,-1.));
#4494=DIRECTION('ref_axis',(1.,0.,0.));
#4495=DIRECTION('center_axis',(0.,0.,1.));
#4496=DIRECTION('ref_axis',(1.,0.,0.));
#4497=DIRECTION('center_axis',(0.,-1.,0.));
#4498=DIRECTION('ref_axis',(1.,0.,0.));
#4499=DIRECTION('',(0.,0.,1.));
#4500=DIRECTION('',(-1.,0.,0.));
#4501=DIRECTION('center_axis',(0.,0.,1.));
#4502=DIRECTION('ref_axis',(0.,1.,0.));
#4503=DIRECTION('center_axis',(1.,0.,0.));
#4504=DIRECTION('ref_axis',(0.,0.,1.));
#4505=DIRECTION('center_axis',(-1.,0.,0.));
#4506=DIRECTION('ref_axis',(0.,0.,1.));
#4507=DIRECTION('center_axis',(-1.,0.,0.));
#4508=DIRECTION('ref_axis',(0.,0.,1.));
#4509=DIRECTION('',(-0.707106781186548,-8.65956056235493E-17,0.707106781186548));
#4510=DIRECTION('center_axis',(1.,0.,0.));
#4511=DIRECTION('ref_axis',(0.,0.,1.));
#4512=DIRECTION('center_axis',(-1.,0.,0.));
#4513=DIRECTION('ref_axis',(0.,0.,1.));
#4514=DIRECTION('center_axis',(1.,0.,0.));
#4515=DIRECTION('ref_axis',(0.,0.,-1.));
#4516=DIRECTION('center_axis',(1.,0.,0.));
#4517=DIRECTION('ref_axis',(0.,0.,-1.));
#4518=DIRECTION('center_axis',(1.,0.,0.));
#4519=DIRECTION('ref_axis',(0.,0.,-1.));
#4520=DIRECTION('',(-1.,0.,0.));
#4521=DIRECTION('center_axis',(1.,0.,0.));
#4522=DIRECTION('ref_axis',(0.,0.,-1.));
#4523=DIRECTION('center_axis',(-1.,0.,0.));
#4524=DIRECTION('ref_axis',(0.,1.22464679914735E-16,1.));
#4525=DIRECTION('center_axis',(0.,-1.,-1.22464679914735E-16));
#4526=DIRECTION('ref_axis',(0.,-1.22464679914735E-16,1.));
#4527=DIRECTION('center_axis',(1.,0.,0.));
#4528=DIRECTION('ref_axis',(0.,1.22464679914735E-16,1.));
#4529=DIRECTION('center_axis',(1.,0.,0.));
#4530=DIRECTION('ref_axis',(0.,0.,-1.));
#4531=DIRECTION('',(-1.,0.,0.));
#4532=DIRECTION('',(-1.,0.,0.));
#4533=DIRECTION('',(-1.,0.,0.));
#4534=DIRECTION('center_axis',(-1.,0.,0.));
#4535=DIRECTION('ref_axis',(0.,1.22464679914735E-16,1.));
#4536=DIRECTION('center_axis',(1.,0.,0.));
#4537=DIRECTION('ref_axis',(0.,0.,-1.));
#4538=DIRECTION('center_axis',(1.,0.,0.));
#4539=DIRECTION('ref_axis',(0.,0.,-1.));
#4540=DIRECTION('center_axis',(0.,-1.,-1.22464679914735E-16));
#4541=DIRECTION('ref_axis',(0.,-1.22464679914735E-16,1.));
#4542=DIRECTION('center_axis',(1.,0.,0.));
#4543=DIRECTION('ref_axis',(0.,1.22464679914735E-16,1.));
#4544=DIRECTION('center_axis',(-1.,0.,0.));
#4545=DIRECTION('ref_axis',(0.,0.,1.));
#4546=DIRECTION('center_axis',(1.,0.,0.));
#4547=DIRECTION('ref_axis',(0.,0.,-1.));
#4548=DIRECTION('center_axis',(1.,0.,0.));
#4549=DIRECTION('ref_axis',(0.,0.,-1.));
#4550=DIRECTION('center_axis',(1.,0.,0.));
#4551=DIRECTION('ref_axis',(0.,0.,-1.));
#4552=DIRECTION('',(-1.,0.,0.));
#7022=CARTESIAN_POINT('',(0.,0.,0.));
#7023=CARTESIAN_POINT('Origin',(21.2197085942866,0.,0.));
#7024=CARTESIAN_POINT('',(30.0128737835214,9.5056654627527,-6.92688080986705E-16));
#7025=CARTESIAN_POINT('',(30.0129125498419,-1.16410452817968E-15,9.50563484084649));
#7026=CARTESIAN_POINT('Origin',(30.0129125498419,0.,0.));
#7027=CARTESIAN_POINT('Origin',(30.0129125498419,0.,0.));
#7028=CARTESIAN_POINT('',(14.0227085942866,9.50563484084649,-5.82052264084792E-16));
#7029=CARTESIAN_POINT('',(21.2197085942866,9.50579594738959,-1.16412425803185E-15));
#7030=CARTESIAN_POINT('',(14.0227085942866,1.16410452817062E-15,9.50563484084649));
#7031=CARTESIAN_POINT('Origin',(14.0227085942866,0.,0.));
#7032=CARTESIAN_POINT('Origin',(14.0227085942866,0.,0.));
#7033=CARTESIAN_POINT('',(27.1076139360583,-1.,9.45305012117298));
#7034=CARTESIAN_POINT('',(16.509210476167,-1.,9.45305012117298));
#7035=CARTESIAN_POINT('',(21.2197085942866,-1.,9.45305012117298));
#7036=CARTESIAN_POINT('',(27.1076139360583,1.,9.45305012117298));
#7037=CARTESIAN_POINT('Ctrl Pts',(27.1076139360583,1.,9.45305012117297));
#7038=CARTESIAN_POINT('Ctrl Pts',(27.2332762619206,1.,9.45305012117297));
#7039=CARTESIAN_POINT('Ctrl Pts',(27.3672506399949,0.974867302313412,9.45581410516793));
#7040=CARTESIAN_POINT('Ctrl Pts',(27.6136022144272,0.872784825785775,9.46578223306855));
#7041=CARTESIAN_POINT('Ctrl Pts',(27.7259873812924,0.795840117138944,9.47284078387221));
#7042=CARTESIAN_POINT('Ctrl Pts',(27.9034536829199,0.618373815511396,9.48607862959468));
#7043=CARTESIAN_POINT('Ctrl Pts',(27.9803986808371,0.505988486616992,9.49312009999403));
#7044=CARTESIAN_POINT('Ctrl Pts',(28.0824813722535,0.259636368087859,9.50304911791651));
#7045=CARTESIAN_POINT('Ctrl Pts',(28.1076139360583,0.125661801483354,9.50579594738959));
#7046=CARTESIAN_POINT('Ctrl Pts',(28.1076139360583,-0.125661801483354,9.5057959473896));
#7047=CARTESIAN_POINT('Ctrl Pts',(28.0824813722535,-0.259636368087854,9.50304911791651));
#7048=CARTESIAN_POINT('Ctrl Pts',(27.9803986808371,-0.505988486616989,9.49312009999403));
#7049=CARTESIAN_POINT('Ctrl Pts',(27.9034536829199,-0.618373815511396,9.48607862959468));
#7050=CARTESIAN_POINT('Ctrl Pts',(27.7259873812924,-0.795840117138944,9.47284078387221));
#7051=CARTESIAN_POINT('Ctrl Pts',(27.6136022144272,-0.872784825785776,9.46578223306855));
#7052=CARTESIAN_POINT('Ctrl Pts',(27.3672506399949,-0.974867302313412,9.45581410516794));
#7053=CARTESIAN_POINT('Ctrl Pts',(27.2332762619206,-1.,9.45305012117297));
#7054=CARTESIAN_POINT('Ctrl Pts',(27.1076139360583,-1.,9.45305012117297));
#7055=CARTESIAN_POINT('',(16.509210476167,1.,9.45305012117298));
#7056=CARTESIAN_POINT('',(21.2197085942866,1.,9.45305012117298));
#7057=CARTESIAN_POINT('Ctrl Pts',(16.509210476167,-1.,9.45305012117298));
#7058=CARTESIAN_POINT('Ctrl Pts',(16.3835481503047,-1.,9.45305012117298));
#7059=CARTESIAN_POINT('Ctrl Pts',(16.2495737722304,-0.974867302313413,9.45581410516794));
#7060=CARTESIAN_POINT('Ctrl Pts',(16.0032221977981,-0.872784825785775,9.46578223306855));
#7061=CARTESIAN_POINT('Ctrl Pts',(15.8908370309329,-0.795840117138944,9.47284078387221));
#7062=CARTESIAN_POINT('Ctrl Pts',(15.7133707293053,-0.618373815511396,9.48607862959468));
#7063=CARTESIAN_POINT('Ctrl Pts',(15.6364257313882,-0.505988486616992,9.49312009999403));
#7064=CARTESIAN_POINT('Ctrl Pts',(15.5343430399718,-0.259636368087859,9.50304911791651));
#7065=CARTESIAN_POINT('Ctrl Pts',(15.509210476167,-0.125661801483353,9.50579594738959));
#7066=CARTESIAN_POINT('Ctrl Pts',(15.509210476167,0.125661801483353,9.50579594738959));
#7067=CARTESIAN_POINT('Ctrl Pts',(15.5343430399718,0.259636368087859,9.50304911791651));
#7068=CARTESIAN_POINT('Ctrl Pts',(15.6364257313882,0.505988486616992,9.49312009999403));
#7069=CARTESIAN_POINT('Ctrl Pts',(15.7133707293053,0.618373815511395,9.48607862959468));
#7070=CARTESIAN_POINT('Ctrl Pts',(15.8908370309329,0.795840117138943,9.47284078387221));
#7071=CARTESIAN_POINT('Ctrl Pts',(16.0032221977981,0.872784825785773,9.46578223306855));
#7072=CARTESIAN_POINT('Ctrl Pts',(16.2495737722303,0.974867302313412,9.45581410516794));
#7073=CARTESIAN_POINT('Ctrl Pts',(16.3835481503047,1.,9.45305012117297));
#7074=CARTESIAN_POINT('Ctrl Pts',(16.509210476167,1.,9.45305012117297));
#7075=CARTESIAN_POINT('Origin',(27.1076139360583,1.,0.));
#7076=CARTESIAN_POINT('',(27.1076139360583,1.,10.9791881928495));
#7077=CARTESIAN_POINT('',(27.1076139360583,1.,0.));
#7078=CARTESIAN_POINT('',(16.509210476167,1.,10.9791881928495));
#7079=CARTESIAN_POINT('',(20.0171174336818,1.,10.9791881928495));
#7080=CARTESIAN_POINT('',(16.509210476167,1.,0.));
#7081=CARTESIAN_POINT('Origin',(27.1076139360583,0.,0.));
#7082=CARTESIAN_POINT('',(27.1076139360583,-1.,10.9791881928495));
#7083=CARTESIAN_POINT('',(27.1076139360583,-1.,0.));
#7084=CARTESIAN_POINT('',(28.1076139360583,-6.9241142324032E-16,11.0246348408465));
#7085=CARTESIAN_POINT('Ctrl Pts',(28.1076139360583,-1.38777878078145E-16,
11.0246348408465));
#7086=CARTESIAN_POINT('Ctrl Pts',(28.1076139360583,-0.125636205005722,11.0246348408465));
#7087=CARTESIAN_POINT('Ctrl Pts',(28.0824913810873,-0.259599701677183,11.0222671389354));
#7088=CARTESIAN_POINT('Ctrl Pts',(27.9804161707035,-0.505958788131831,11.0137083033886));
#7089=CARTESIAN_POINT('Ctrl Pts',(27.9034673289024,-0.618360169528907,11.00763882809));
#7090=CARTESIAN_POINT('Ctrl Pts',(27.7259739014455,-0.795853596985864,10.9962311251393));
#7091=CARTESIAN_POINT('Ctrl Pts',(27.6135726098982,-0.872802279941483,10.9901507178533));
#7092=CARTESIAN_POINT('Ctrl Pts',(27.3672138227875,-0.974877370414414,10.9815668619283));
#7093=CARTESIAN_POINT('Ctrl Pts',(27.2332504300619,-1.,10.9791881928495));
#7094=CARTESIAN_POINT('Ctrl Pts',(27.1076139360583,-1.,10.9791881928495));
#7095=CARTESIAN_POINT('Ctrl Pts',(27.1076139360583,1.,10.9791881928495));
#7096=CARTESIAN_POINT('Ctrl Pts',(27.2332504300619,1.,10.9791881928495));
#7097=CARTESIAN_POINT('Ctrl Pts',(27.3672138227875,0.974877370414413,10.9815668619283));
#7098=CARTESIAN_POINT('Ctrl Pts',(27.6135726098982,0.87280227994148,10.9901507178533));
#7099=CARTESIAN_POINT('Ctrl Pts',(27.7259739014455,0.795853596985865,10.9962311251393));
#7100=CARTESIAN_POINT('Ctrl Pts',(27.9034673289024,0.618360169528908,11.00763882809));
#7101=CARTESIAN_POINT('Ctrl Pts',(27.9804161707035,0.505958788131831,11.0137083033886));
#7102=CARTESIAN_POINT('Ctrl Pts',(28.0824913810873,0.259599701677183,11.0222671389354));
#7103=CARTESIAN_POINT('Ctrl Pts',(28.1076139360583,0.125636205005722,11.0246348408465));
#7104=CARTESIAN_POINT('Ctrl Pts',(28.1076139360583,-6.93889390390723E-17,
11.0246348408465));
#7105=CARTESIAN_POINT('Origin',(12.8302991238869,0.,12.));
#7106=CARTESIAN_POINT('',(12.8302991238869,1.,10.9791881928495));
#7107=CARTESIAN_POINT('',(13.8302991238869,-5.70980779921944E-16,11.0246348408465));
#7108=CARTESIAN_POINT('Ctrl Pts',(12.8302991238869,1.,10.9791881928495));
#7109=CARTESIAN_POINT('Ctrl Pts',(12.9559356178906,1.,10.9791881928495));
#7110=CARTESIAN_POINT('Ctrl Pts',(13.0898990106162,0.974877370414413,10.9815668619283));
#7111=CARTESIAN_POINT('Ctrl Pts',(13.3362577977268,0.87280227994148,10.9901507178533));
#7112=CARTESIAN_POINT('Ctrl Pts',(13.4486590892742,0.795853596985866,10.9962311251393));
#7113=CARTESIAN_POINT('Ctrl Pts',(13.6261525167311,0.618360169528908,11.00763882809));
#7114=CARTESIAN_POINT('Ctrl Pts',(13.7031013585322,0.505958788131832,11.0137083033886));
#7115=CARTESIAN_POINT('Ctrl Pts',(13.805176568916,0.259599701677187,11.0222671389354));
#7116=CARTESIAN_POINT('Ctrl Pts',(13.8302991238869,0.125636205005722,11.0246348408465));
#7117=CARTESIAN_POINT('Ctrl Pts',(13.8302991238869,-3.46944695195361E-17,
11.0246348408465));
#7118=CARTESIAN_POINT('',(11.8302991238869,1.22464679914735E-16,11.0246348408465));
#7119=CARTESIAN_POINT('Ctrl Pts',(11.8302991238869,-1.38777878078145E-16,
11.0246348408465));
#7120=CARTESIAN_POINT('Ctrl Pts',(11.8302991238869,0.125636205005722,11.0246348408465));
#7121=CARTESIAN_POINT('Ctrl Pts',(11.8554216788579,0.259599701677188,11.0222671389354));
#7122=CARTESIAN_POINT('Ctrl Pts',(11.9574968892417,0.505958788131833,11.0137083033886));
#7123=CARTESIAN_POINT('Ctrl Pts',(12.0344457310427,0.618360169528908,11.00763882809));
#7124=CARTESIAN_POINT('Ctrl Pts',(12.2119391584997,0.795853596985866,10.9962311251393));
#7125=CARTESIAN_POINT('Ctrl Pts',(12.324340450047,0.87280227994148,10.9901507178533));
#7126=CARTESIAN_POINT('Ctrl Pts',(12.5706992371577,0.974877370414413,10.9815668619283));
#7127=CARTESIAN_POINT('Ctrl Pts',(12.7046626298833,1.,10.9791881928495));
#7128=CARTESIAN_POINT('Ctrl Pts',(12.8302991238869,1.,10.9791881928495));
#7129=CARTESIAN_POINT('',(11.8302991238869,-1.22464679914735E-16,10.));
#7130=CARTESIAN_POINT('',(11.8302991238869,1.22464679914735E-16,12.));
#7131=CARTESIAN_POINT('Origin',(12.8302991238869,0.,10.));
#7132=CARTESIAN_POINT('Ctrl Pts',(13.8302991238869,2.77555756156289E-16,
11.0246348408465));
#7133=CARTESIAN_POINT('Ctrl Pts',(13.8302991238869,-0.125636205005722,11.0246348408465));
#7134=CARTESIAN_POINT('Ctrl Pts',(13.805176568916,-0.259599701677187,11.0222671389354));
#7135=CARTESIAN_POINT('Ctrl Pts',(13.7031013585322,-0.505958788131832,11.0137083033886));
#7136=CARTESIAN_POINT('Ctrl Pts',(13.6261525167311,-0.618360169528908,11.00763882809));
#7137=CARTESIAN_POINT('Ctrl Pts',(13.4486590892742,-0.795853596985866,10.9962311251393));
#7138=CARTESIAN_POINT('Ctrl Pts',(13.3362577977268,-0.87280227994148,10.9901507178533));
#7139=CARTESIAN_POINT('Ctrl Pts',(13.0898990106162,-0.974877370414413,10.9815668619283));
#7140=CARTESIAN_POINT('Ctrl Pts',(12.9559356178906,-1.,10.9791881928495));
#7141=CARTESIAN_POINT('Ctrl Pts',(12.7046626298833,-1.,10.9791881928495));
#7142=CARTESIAN_POINT('Ctrl Pts',(12.5706992371577,-0.974877370414413,10.9815668619283));
#7143=CARTESIAN_POINT('Ctrl Pts',(12.324340450047,-0.87280227994148,10.9901507178533));
#7144=CARTESIAN_POINT('Ctrl Pts',(12.2119391584997,-0.795853596985866,10.9962311251393));
#7145=CARTESIAN_POINT('Ctrl Pts',(12.0344457310427,-0.618360169528909,11.00763882809));
#7146=CARTESIAN_POINT('Ctrl Pts',(11.9574968892417,-0.505958788131833,11.0137083033886));
#7147=CARTESIAN_POINT('Ctrl Pts',(11.8554216788579,-0.259599701677187,11.0222671389354));
#7148=CARTESIAN_POINT('Ctrl Pts',(11.8302991238869,-0.125636205005722,11.0246348408465));
#7149=CARTESIAN_POINT('Ctrl Pts',(11.8302991238869,-6.93889390390723E-17,
11.0246348408465));
#7150=CARTESIAN_POINT('Origin',(12.8302991238869,0.,10.));
#7151=CARTESIAN_POINT('Origin',(16.509210476167,-1.,0.));
#7152=CARTESIAN_POINT('',(16.509210476167,-1.,10.9791881928495));
#7153=CARTESIAN_POINT('',(16.509210476167,-1.,0.));
#7154=CARTESIAN_POINT('',(20.0171174336818,-1.,10.9791881928495));
#7155=CARTESIAN_POINT('Origin',(16.509210476167,0.,0.));
#7156=CARTESIAN_POINT('',(15.509210476167,-7.79147597039161E-16,11.0246348408465));
#7157=CARTESIAN_POINT('Ctrl Pts',(15.509210476167,-1.73472347597681E-16,
11.0246348408465));
#7158=CARTESIAN_POINT('Ctrl Pts',(15.509210476167,0.125636205005722,11.0246348408465));
#7159=CARTESIAN_POINT('Ctrl Pts',(15.534333031138,0.259599701677186,11.0222671389354));
#7160=CARTESIAN_POINT('Ctrl Pts',(15.6364082415218,0.505958788131832,11.0137083033886));
#7161=CARTESIAN_POINT('Ctrl Pts',(15.7133570833229,0.618360169528908,11.00763882809));
#7162=CARTESIAN_POINT('Ctrl Pts',(15.8908505107798,0.795853596985865,10.9962311251393));
#7163=CARTESIAN_POINT('Ctrl Pts',(16.0032518023271,0.87280227994148,10.9901507178533));
#7164=CARTESIAN_POINT('Ctrl Pts',(16.2496105894378,0.974877370414413,10.9815668619283));
#7165=CARTESIAN_POINT('Ctrl Pts',(16.3835739821634,1.,10.9791881928495));
#7166=CARTESIAN_POINT('Ctrl Pts',(16.509210476167,1.,10.9791881928495));
#7167=CARTESIAN_POINT('Ctrl Pts',(16.509210476167,-1.,10.9791881928495));
#7168=CARTESIAN_POINT('Ctrl Pts',(16.3835739821634,-1.,10.9791881928495));
#7169=CARTESIAN_POINT('Ctrl Pts',(16.2496105894378,-0.974877370414412,10.9815668619283));
#7170=CARTESIAN_POINT('Ctrl Pts',(16.0032518023271,-0.872802279941479,10.9901507178533));
#7171=CARTESIAN_POINT('Ctrl Pts',(15.8908505107798,-0.795853596985865,10.9962311251393));
#7172=CARTESIAN_POINT('Ctrl Pts',(15.7133570833228,-0.618360169528908,11.00763882809));
#7173=CARTESIAN_POINT('Ctrl Pts',(15.6364082415218,-0.505958788131831,11.0137083033886));
#7174=CARTESIAN_POINT('Ctrl Pts',(15.534333031138,-0.259599701677186,11.0222671389354));
#7175=CARTESIAN_POINT('Ctrl Pts',(15.509210476167,-0.125636205005722,11.0246348408465));
#7176=CARTESIAN_POINT('Ctrl Pts',(15.509210476167,2.08166817117217E-16,
11.0246348408465));
#7177=CARTESIAN_POINT('Origin',(0.25,0.,0.));
#7178=CARTESIAN_POINT('',(0.5,-5.78383980645509E-16,-4.72286361298787));
#7179=CARTESIAN_POINT('',(0.5,-5.78383980645509E-16,4.72286361298787));
#7180=CARTESIAN_POINT('Origin',(0.5,0.,0.));
#7181=CARTESIAN_POINT('Origin',(0.5,0.,0.));
#7182=CARTESIAN_POINT('',(0.,5.17151640688142E-16,-4.22286361298787));
#7183=CARTESIAN_POINT('',(0.25,5.47767810666826E-16,-4.47286361298787));
#7184=CARTESIAN_POINT('Origin',(0.,0.,0.));
#7185=CARTESIAN_POINT('Origin',(0.,0.,-4.72286361298787));
#7186=CARTESIAN_POINT('',(0.,-4.55919300730774E-16,3.72286361298787));
#7187=CARTESIAN_POINT('Origin',(0.,0.,0.));
#7188=CARTESIAN_POINT('Origin',(5.01066115876088,0.,0.));
#7189=CARTESIAN_POINT('',(10.0213223175218,-5.78383980645509E-16,4.72286361298787));
#7190=CARTESIAN_POINT('Origin',(10.0213223175218,0.,0.));
#7191=CARTESIAN_POINT('',(5.01066115876088,-5.78383980645509E-16,4.72286361298787));
#7192=CARTESIAN_POINT('Origin',(29.5129125498419,0.,0.));
#7193=CARTESIAN_POINT('',(30.0129125498419,-1.28889603700374E-15,10.5246348408465));
#7194=CARTESIAN_POINT('Origin',(30.0129125498419,0.,0.));
#7195=CARTESIAN_POINT('',(29.5129125498419,-1.3501283769611E-15,11.0246348408465));
#7196=CARTESIAN_POINT('Origin',(29.5129125498419,-1.28889603700374E-15,
10.5246348408465));
#7197=CARTESIAN_POINT('Origin',(29.5129125498419,0.,0.));
#7198=CARTESIAN_POINT('Origin',(20.0171174336818,0.,0.));
#7199=CARTESIAN_POINT('',(20.0171174336818,-1.3501283769611E-15,11.0246348408465));
#7200=CARTESIAN_POINT('',(20.0171174336818,-1.3501283769611E-15,11.0246348408465));
#7201=CARTESIAN_POINT('',(10.5213223175218,-1.3501283769611E-15,11.0246348408465));
#7202=CARTESIAN_POINT('',(20.0171174336818,-1.3501283769611E-15,11.0246348408465));
#7203=CARTESIAN_POINT('Origin',(10.5213223175218,0.,0.));
#7204=CARTESIAN_POINT('Origin',(30.0129125498419,0.,-10.0246348408465));
#7205=CARTESIAN_POINT('Origin',(10.5213223175218,0.,0.));
#7206=CARTESIAN_POINT('',(10.0213223175218,-1.28889603700374E-15,10.5246348408465));
#7207=CARTESIAN_POINT('Origin',(10.5213223175218,-1.28889603700374E-15,
10.5246348408465));
#7208=CARTESIAN_POINT('Origin',(10.0213223175218,0.,0.));
#7209=CARTESIAN_POINT('Origin',(10.0213223175218,0.,-11.0246348408465));
#7210=CARTESIAN_POINT('Origin',(14.0224984115252,0.,-3.72286361298787));
#7211=CARTESIAN_POINT('',(14.0224984115252,-4.55919300730774E-16,3.72286361298787));
#7212=CARTESIAN_POINT('Origin',(14.0224984115252,0.,0.));
#7213=CARTESIAN_POINT('Origin',(7.01124920576262,0.,0.));
#7214=CARTESIAN_POINT('',(7.01124920576262,-4.55919300730774E-16,3.72286361298787));
#7297=UNCERTAINTY_MEASURE_WITH_UNIT(LENGTH_MEASURE(0.01),#7316,
'DISTANCE_ACCURACY_VALUE',
'Maximum model space distance between geometric entities at asserted c
onnectivities');
#7303=UNCERTAINTY_MEASURE_WITH_UNIT(LENGTH_MEASURE(0.01),#7316,
'DISTANCE_ACCURACY_VALUE',
'Maximum model space distance between geometric entities at asserted c
onnectivities');
#7309=(
GEOMETRIC_REPRESENTATION_CONTEXT(3)
GLOBAL_UNCERTAINTY_ASSIGNED_CONTEXT((#7297))
GLOBAL_UNIT_ASSIGNED_CONTEXT((#7316,#7318,#7319))
REPRESENTATION_CONTEXT('','3D')
);
#7315=(
GEOMETRIC_REPRESENTATION_CONTEXT(3)
GLOBAL_UNCERTAINTY_ASSIGNED_CONTEXT((#7303))
GLOBAL_UNIT_ASSIGNED_CONTEXT((#7316,#7318,#7319))
REPRESENTATION_CONTEXT('','3D')
);
#7316=(
LENGTH_UNIT()
NAMED_UNIT(*)
SI_UNIT(.MILLI.,.METRE.)
);
#7318=(
NAMED_UNIT(*)
PLANE_ANGLE_UNIT()
SI_UNIT($,.RADIAN.)
);
#7319=(
NAMED_UNIT(*)
SI_UNIT($,.STERADIAN.)
SOLID_ANGLE_UNIT()
);
#7325=SHAPE_DEFINITION_REPRESENTATION(#7336,#7357);
#7336=PRODUCT_DEFINITION_SHAPE('',$,#7369);
#7357=SHAPE_REPRESENTATION('',(#3638),#7309);
#7363=PRODUCT_DEFINITION_CONTEXT('part definition',#7398,'design');
#7369=PRODUCT_DEFINITION('Main_Housing','Main_Housing',#7380,#7363);
#7380=PRODUCT_DEFINITION_FORMATION('',$,#7405);
#7398=APPLICATION_CONTEXT(
'Core Data for Automotive Mechanical Design Process');
#7399=PRODUCT_CONTEXT('part definition',#7398,'mechanical');
#7405=PRODUCT('Main_Housing','Main_Housing',$,(#7399));
#7418=COLOUR_RGB('Dark Blue',0.08,0.2,0.34);
#7419=FILL_AREA_STYLE_COLOUR('',#7418);
#7420=FILL_AREA_STYLE('',(#7419));
#7421=SURFACE_STYLE_FILL_AREA(#7420);
#7422=SURFACE_SIDE_STYLE('',(#7421));
#7423=SURFACE_STYLE_USAGE(.BOTH.,#7422);
#7424=PRESENTATION_STYLE_ASSIGNMENT((#7423));
ENDSEC;
END-ISO-10303-21;
